ISO-10303-21;
HEADER;
/* Generated by software containing ST-Developer
 * from STEP Tools, Inc. (www.steptools.com) 
 */

FILE_DESCRIPTION(
/* description */ ('PAT-015'),
/* implementation_level */ '2;1');

FILE_NAME(
/* name */ 'Cap Screw - M4x16.step',
/* time_stamp */ '2026-10-29T16:03:43-07:00',
/* author */ (''),
/* organization */ (''),
/* preprocessor_version */ 'ST-DEVELOPER v20.2',
/* originating_system */ 'Autodesk Translation Framework v15.17.0.0',
/* authorisation */ '');

FILE_SCHEMA (('AUTOMOTIVE_DESIGN { 1 0 10303 214 3 1 1 }'));
ENDSEC;

DATA;
#10=MECHANICAL_DESIGN_GEOMETRIC_PRESENTATION_REPRESENTATION('',(#254),#10266);
#164=ORIENTED_CLOSED_SHELL('',*,#4715,.F.);
#166=BREP_WITH_VOIDS('Body1',#4714,(#164));
#178=CONICAL_SURFACE('',#5498,0.325,0.785398163397448);
#179=CONICAL_SURFACE('',#5502,0.335,0.785398163397448);
#180=CONICAL_SURFACE('',#5506,0.21,0.463647609000806);
#181=CONICAL_SURFACE('',#5510,0.18,0.785398163397448);
#206=SHAPE_REPRESENTATION_RELATIONSHIP('SRR','None',#10377,#229);
#229=ADVANCED_BREP_SHAPE_REPRESENTATION('',(#166),#10265);
#254=STYLED_ITEM('',(#10554),#166);
#419=FACE_BOUND('',#1252,.T.);
#560=PLANE('',#5496);
#561=PLANE('',#5504);
#562=PLANE('',#5512);
#563=PLANE('',#5513);
#564=PLANE('',#5514);
#565=PLANE('',#5515);
#566=PLANE('',#5516);
#567=PLANE('',#5517);
#568=PLANE('',#5518);
#569=PLANE('',#5519);
#570=PLANE('',#5520);
#837=FACE_OUTER_BOUND('',#1247,.T.);
#838=FACE_OUTER_BOUND('',#1248,.T.);
#839=FACE_OUTER_BOUND('',#1249,.T.);
#840=FACE_OUTER_BOUND('',#1250,.T.);
#841=FACE_OUTER_BOUND('',#1251,.T.);
#842=FACE_OUTER_BOUND('',#1253,.T.);
#843=FACE_OUTER_BOUND('',#1254,.T.);
#844=FACE_OUTER_BOUND('',#1255,.T.);
#845=FACE_OUTER_BOUND('',#1256,.T.);
#846=FACE_OUTER_BOUND('',#1257,.T.);
#847=FACE_OUTER_BOUND('',#1258,.T.);
#848=FACE_OUTER_BOUND('',#1259,.T.);
#849=FACE_OUTER_BOUND('',#1260,.T.);
#850=FACE_OUTER_BOUND('',#1261,.T.);
#851=FACE_OUTER_BOUND('',#1262,.T.);
#852=FACE_OUTER_BOUND('',#1263,.T.);
#853=FACE_OUTER_BOUND('',#1264,.T.);
#1247=EDGE_LOOP('',(#4227));
#1248=EDGE_LOOP('',(#4228,#4229,#4230,#4231));
#1249=EDGE_LOOP('',(#4232,#4233,#4234,#4235));
#1250=EDGE_LOOP('',(#4236,#4237,#4238,#4239));
#1251=EDGE_LOOP('',(#4240));
#1252=EDGE_LOOP('',(#4241));
#1253=EDGE_LOOP('',(#4242,#4243,#4244,#4245));
#1254=EDGE_LOOP('',(#4246,#4247,#4248,#4249));
#1255=EDGE_LOOP('',(#4250,#4251,#4252,#4253));
#1256=EDGE_LOOP('',(#4254));
#1257=EDGE_LOOP('',(#4255,#4256,#4257,#4258));
#1258=EDGE_LOOP('',(#4259,#4260,#4261,#4262));
#1259=EDGE_LOOP('',(#4263,#4264,#4265,#4266));
#1260=EDGE_LOOP('',(#4267,#4268,#4269,#4270));
#1261=EDGE_LOOP('',(#4271,#4272,#4273,#4274));
#1262=EDGE_LOOP('',(#4275,#4276,#4277,#4278));
#1263=EDGE_LOOP('',(#4279,#4280,#4281,#4282,#4283,#4284));
#1264=EDGE_LOOP('',(#4285,#4286,#4287,#4288,#4289,#4290));
#1579=LINE('',#10119,#1859);
#1580=LINE('',#10123,#1860);
#1581=LINE('',#10127,#1861);
#1582=LINE('',#10134,#1862);
#1583=LINE('',#10138,#1863);
#1584=LINE('',#10142,#1864);
#1585=LINE('',#10147,#1865);
#1586=LINE('',#10149,#1866);
#1587=LINE('',#10151,#1867);
#1588=LINE('',#10152,#1868);
#1589=LINE('',#10155,#1869);
#1590=LINE('',#10157,#1870);
#1591=LINE('',#10158,#1871);
#1592=LINE('',#10161,#1872);
#1593=LINE('',#10163,#1873);
#1594=LINE('',#10164,#1874);
#1595=LINE('',#10167,#1875);
#1596=LINE('',#10169,#1876);
#1597=LINE('',#10170,#1877);
#1598=LINE('',#10173,#1878);
#1599=LINE('',#10175,#1879);
#1600=LINE('',#10176,#1880);
#1601=LINE('',#10178,#1881);
#1602=LINE('',#10179,#1882);
#1859=VECTOR('',#6872,0.325);
#1860=VECTOR('',#6877,0.35);
#1861=VECTOR('',#6882,0.335);
#1862=VECTOR('',#6891,0.21);
#1863=VECTOR('',#6896,0.2);
#1864=VECTOR('',#6901,0.18);
#1865=VECTOR('',#6906,1.);
#1866=VECTOR('',#6907,1.);
#1867=VECTOR('',#6908,1.);
#1868=VECTOR('',#6909,1.);
#1869=VECTOR('',#6912,1.);
#1870=VECTOR('',#6913,1.);
#1871=VECTOR('',#6914,1.);
#1872=VECTOR('',#6917,1.);
#1873=VECTOR('',#6918,1.);
#1874=VECTOR('',#6919,1.);
#1875=VECTOR('',#6922,1.);
#1876=VECTOR('',#6923,1.);
#1877=VECTOR('',#6924,1.);
#1878=VECTOR('',#6927,1.);
#1879=VECTOR('',#6928,1.);
#1880=VECTOR('',#6929,1.);
#1881=VECTOR('',#6932,1.);
#1882=VECTOR('',#6933,1.);
#2106=CIRCLE('',#5497,0.3);
#2107=CIRCLE('',#5499,0.35);
#2108=CIRCLE('',#5501,0.35);
#2109=CIRCLE('',#5503,0.32);
#2110=CIRCLE('',#5505,0.22);
#2111=CIRCLE('',#5507,0.1954);
#2112=CIRCLE('',#5509,0.1954);
#2113=CIRCLE('',#5511,0.16);
#2486=VERTEX_POINT('',#10114);
#2487=VERTEX_POINT('',#10117);
#2488=VERTEX_POINT('',#10121);
#2489=VERTEX_POINT('',#10125);
#2490=VERTEX_POINT('',#10129);
#2491=VERTEX_POINT('',#10132);
#2492=VERTEX_POINT('',#10136);
#2493=VERTEX_POINT('',#10140);
#2494=VERTEX_POINT('',#10145);
#2495=VERTEX_POINT('',#10146);
#2496=VERTEX_POINT('',#10148);
#2497=VERTEX_POINT('',#10150);
#2498=VERTEX_POINT('',#10154);
#2499=VERTEX_POINT('',#10156);
#2500=VERTEX_POINT('',#10160);
#2501=VERTEX_POINT('',#10162);
#2502=VERTEX_POINT('',#10166);
#2503=VERTEX_POINT('',#10168);
#2504=VERTEX_POINT('',#10172);
#2505=VERTEX_POINT('',#10174);
#3069=EDGE_CURVE('',#2486,#2486,#2106,.T.);
#3070=EDGE_CURVE('',#2487,#2487,#2107,.T.);
#3071=EDGE_CURVE('',#2487,#2486,#1579,.T.);
#3072=EDGE_CURVE('',#2488,#2488,#2108,.T.);
#3073=EDGE_CURVE('',#2488,#2487,#1580,.T.);
#3074=EDGE_CURVE('',#2489,#2489,#2109,.T.);
#3075=EDGE_CURVE('',#2489,#2488,#1581,.T.);
#3076=EDGE_CURVE('',#2490,#2490,#2110,.T.);
#3077=EDGE_CURVE('',#2491,#2491,#2111,.F.);
#3078=EDGE_CURVE('',#2491,#2490,#1582,.T.);
#3079=EDGE_CURVE('',#2492,#2492,#2112,.F.);
#3080=EDGE_CURVE('',#2492,#2491,#1583,.T.);
#3081=EDGE_CURVE('',#2493,#2493,#2113,.T.);
#3082=EDGE_CURVE('',#2493,#2492,#1584,.T.);
#3083=EDGE_CURVE('',#2494,#2495,#1585,.T.);
#3084=EDGE_CURVE('',#2495,#2496,#1586,.T.);
#3085=EDGE_CURVE('',#2496,#2497,#1587,.T.);
#3086=EDGE_CURVE('',#2494,#2497,#1588,.T.);
#3087=EDGE_CURVE('',#2495,#2498,#1589,.T.);
#3088=EDGE_CURVE('',#2498,#2499,#1590,.T.);
#3089=EDGE_CURVE('',#2499,#2496,#1591,.T.);
#3090=EDGE_CURVE('',#2498,#2500,#1592,.T.);
#3091=EDGE_CURVE('',#2500,#2501,#1593,.T.);
#3092=EDGE_CURVE('',#2501,#2499,#1594,.T.);
#3093=EDGE_CURVE('',#2500,#2502,#1595,.T.);
#3094=EDGE_CURVE('',#2502,#2503,#1596,.T.);
#3095=EDGE_CURVE('',#2503,#2501,#1597,.T.);
#3096=EDGE_CURVE('',#2502,#2504,#1598,.T.);
#3097=EDGE_CURVE('',#2504,#2505,#1599,.T.);
#3098=EDGE_CURVE('',#2505,#2503,#1600,.T.);
#3099=EDGE_CURVE('',#2504,#2494,#1601,.T.);
#3100=EDGE_CURVE('',#2497,#2505,#1602,.T.);
#4227=ORIENTED_EDGE('',*,*,#3069,.F.);
#4228=ORIENTED_EDGE('',*,*,#3070,.F.);
#4229=ORIENTED_EDGE('',*,*,#3071,.T.);
#4230=ORIENTED_EDGE('',*,*,#3069,.T.);
#4231=ORIENTED_EDGE('',*,*,#3071,.F.);
#4232=ORIENTED_EDGE('',*,*,#3072,.F.);
#4233=ORIENTED_EDGE('',*,*,#3073,.T.);
#4234=ORIENTED_EDGE('',*,*,#3070,.T.);
#4235=ORIENTED_EDGE('',*,*,#3073,.F.);
#4236=ORIENTED_EDGE('',*,*,#3074,.F.);
#4237=ORIENTED_EDGE('',*,*,#3075,.T.);
#4238=ORIENTED_EDGE('',*,*,#3072,.T.);
#4239=ORIENTED_EDGE('',*,*,#3075,.F.);
#4240=ORIENTED_EDGE('',*,*,#3074,.T.);
#4241=ORIENTED_EDGE('',*,*,#3076,.F.);
#4242=ORIENTED_EDGE('',*,*,#3077,.F.);
#4243=ORIENTED_EDGE('',*,*,#3078,.T.);
#4244=ORIENTED_EDGE('',*,*,#3076,.T.);
#4245=ORIENTED_EDGE('',*,*,#3078,.F.);
#4246=ORIENTED_EDGE('',*,*,#3079,.F.);
#4247=ORIENTED_EDGE('',*,*,#3080,.T.);
#4248=ORIENTED_EDGE('',*,*,#3077,.T.);
#4249=ORIENTED_EDGE('',*,*,#3080,.F.);
#4250=ORIENTED_EDGE('',*,*,#3081,.F.);
#4251=ORIENTED_EDGE('',*,*,#3082,.T.);
#4252=ORIENTED_EDGE('',*,*,#3079,.T.);
#4253=ORIENTED_EDGE('',*,*,#3082,.F.);
#4254=ORIENTED_EDGE('',*,*,#3081,.T.);
#4255=ORIENTED_EDGE('',*,*,#3083,.T.);
#4256=ORIENTED_EDGE('',*,*,#3084,.T.);
#4257=ORIENTED_EDGE('',*,*,#3085,.T.);
#4258=ORIENTED_EDGE('',*,*,#3086,.F.);
#4259=ORIENTED_EDGE('',*,*,#3087,.T.);
#4260=ORIENTED_EDGE('',*,*,#3088,.T.);
#4261=ORIENTED_EDGE('',*,*,#3089,.T.);
#4262=ORIENTED_EDGE('',*,*,#3084,.F.);
#4263=ORIENTED_EDGE('',*,*,#3090,.T.);
#4264=ORIENTED_EDGE('',*,*,#3091,.T.);
#4265=ORIENTED_EDGE('',*,*,#3092,.T.);
#4266=ORIENTED_EDGE('',*,*,#3088,.F.);
#4267=ORIENTED_EDGE('',*,*,#3093,.T.);
#4268=ORIENTED_EDGE('',*,*,#3094,.T.);
#4269=ORIENTED_EDGE('',*,*,#3095,.T.);
#4270=ORIENTED_EDGE('',*,*,#3091,.F.);
#4271=ORIENTED_EDGE('',*,*,#3096,.T.);
#4272=ORIENTED_EDGE('',*,*,#3097,.T.);
#4273=ORIENTED_EDGE('',*,*,#3098,.T.);
#4274=ORIENTED_EDGE('',*,*,#3094,.F.);
#4275=ORIENTED_EDGE('',*,*,#3099,.T.);
#4276=ORIENTED_EDGE('',*,*,#3086,.T.);
#4277=ORIENTED_EDGE('',*,*,#3100,.T.);
#4278=ORIENTED_EDGE('',*,*,#3097,.F.);
#4279=ORIENTED_EDGE('',*,*,#3099,.F.);
#4280=ORIENTED_EDGE('',*,*,#3096,.F.);
#4281=ORIENTED_EDGE('',*,*,#3093,.F.);
#4282=ORIENTED_EDGE('',*,*,#3090,.F.);
#4283=ORIENTED_EDGE('',*,*,#3087,.F.);
#4284=ORIENTED_EDGE('',*,*,#3083,.F.);
#4285=ORIENTED_EDGE('',*,*,#3100,.F.);
#4286=ORIENTED_EDGE('',*,*,#3085,.F.);
#4287=ORIENTED_EDGE('',*,*,#3089,.F.);
#4288=ORIENTED_EDGE('',*,*,#3092,.F.);
#4289=ORIENTED_EDGE('',*,*,#3095,.F.);
#4290=ORIENTED_EDGE('',*,*,#3098,.F.);
#4404=CYLINDRICAL_SURFACE('',#5500,0.35);
#4405=CYLINDRICAL_SURFACE('',#5508,0.1954);
#4672=ADVANCED_FACE('',(#837),#560,.T.);
#4673=ADVANCED_FACE('',(#838),#178,.T.);
#4674=ADVANCED_FACE('',(#839),#4404,.T.);
#4675=ADVANCED_FACE('',(#840),#179,.T.);
#4676=ADVANCED_FACE('',(#841,#419),#561,.T.);
#4677=ADVANCED_FACE('',(#842),#180,.T.);
#4678=ADVANCED_FACE('',(#843),#4405,.T.);
#4679=ADVANCED_FACE('',(#844),#181,.T.);
#4680=ADVANCED_FACE('',(#845),#562,.T.);
#4681=ADVANCED_FACE('',(#846),#563,.F.);
#4682=ADVANCED_FACE('',(#847),#564,.F.);
#4683=ADVANCED_FACE('',(#848),#565,.F.);
#4684=ADVANCED_FACE('',(#849),#566,.F.);
#4685=ADVANCED_FACE('',(#850),#567,.F.);
#4686=ADVANCED_FACE('',(#851),#568,.F.);
#4687=ADVANCED_FACE('',(#852),#569,.F.);
#4688=ADVANCED_FACE('',(#853),#570,.F.);
#4714=CLOSED_SHELL('',(#4672,#4673,#4674,#4675,#4676,#4677,#4678,#4679,
#4680));
#4715=CLOSED_SHELL('',(#4681,#4682,#4683,#4684,#4685,#4686,#4687,#4688));
#5495=AXIS2_PLACEMENT_3D('',#10112,#6862,#6863);
#5496=AXIS2_PLACEMENT_3D('',#10113,#6864,#6865);
#5497=AXIS2_PLACEMENT_3D('',#10115,#6866,#6867);
#5498=AXIS2_PLACEMENT_3D('',#10116,#6868,#6869);
#5499=AXIS2_PLACEMENT_3D('',#10118,#6870,#6871);
#5500=AXIS2_PLACEMENT_3D('',#10120,#6873,#6874);
#5501=AXIS2_PLACEMENT_3D('',#10122,#6875,#6876);
#5502=AXIS2_PLACEMENT_3D('',#10124,#6878,#6879);
#5503=AXIS2_PLACEMENT_3D('',#10126,#6880,#6881);
#5504=AXIS2_PLACEMENT_3D('',#10128,#6883,#6884);
#5505=AXIS2_PLACEMENT_3D('',#10130,#6885,#6886);
#5506=AXIS2_PLACEMENT_3D('',#10131,#6887,#6888);
#5507=AXIS2_PLACEMENT_3D('',#10133,#6889,#6890);
#5508=AXIS2_PLACEMENT_3D('',#10135,#6892,#6893);
#5509=AXIS2_PLACEMENT_3D('',#10137,#6894,#6895);
#5510=AXIS2_PLACEMENT_3D('',#10139,#6897,#6898);
#5511=AXIS2_PLACEMENT_3D('',#10141,#6899,#6900);
#5512=AXIS2_PLACEMENT_3D('',#10143,#6902,#6903);
#5513=AXIS2_PLACEMENT_3D('',#10144,#6904,#6905);
#5514=AXIS2_PLACEMENT_3D('',#10153,#6910,#6911);
#5515=AXIS2_PLACEMENT_3D('',#10159,#6915,#6916);
#5516=AXIS2_PLACEMENT_3D('',#10165,#6920,#6921);
#5517=AXIS2_PLACEMENT_3D('',#10171,#6925,#6926);
#5518=AXIS2_PLACEMENT_3D('',#10177,#6930,#6931);
#5519=AXIS2_PLACEMENT_3D('',#10180,#6934,#6935);
#5520=AXIS2_PLACEMENT_3D('',#10181,#6936,#6937);
#6862=DIRECTION('axis',(0.,0.,1.));
#6863=DIRECTION('refdir',(1.,0.,0.));
#6864=DIRECTION('center_axis',(0.,1.,0.));
#6865=DIRECTION('ref_axis',(0.,0.,1.));
#6866=DIRECTION('center_axis',(0.,-1.,0.));
#6867=DIRECTION('ref_axis',(1.,0.,0.));
#6868=DIRECTION('center_axis',(0.,-1.,0.));
#6869=DIRECTION('ref_axis',(1.,0.,0.));
#6870=DIRECTION('center_axis',(0.,-1.,0.));
#6871=DIRECTION('ref_axis',(1.,0.,0.));
#6872=DIRECTION('',(0.707106781186547,0.707106781186548,8.65956056235493E-17));
#6873=DIRECTION('center_axis',(0.,-1.,0.));
#6874=DIRECTION('ref_axis',(1.,0.,0.));
#6875=DIRECTION('center_axis',(0.,-1.,0.));
#6876=DIRECTION('ref_axis',(1.,0.,0.));
#6877=DIRECTION('',(0.,1.,0.));
#6878=DIRECTION('center_axis',(0.,1.,0.));
#6879=DIRECTION('ref_axis',(1.,0.,0.));
#6880=DIRECTION('center_axis',(0.,-1.,0.));
#6881=DIRECTION('ref_axis',(1.,0.,0.));
#6882=DIRECTION('',(-0.707106781186547,0.707106781186548,-8.65956056235493E-17));
#6883=DIRECTION('center_axis',(0.,-1.,0.));
#6884=DIRECTION('ref_axis',(0.,0.,-1.));
#6885=DIRECTION('center_axis',(0.,-1.,0.));
#6886=DIRECTION('ref_axis',(1.,0.,0.));
#6887=DIRECTION('center_axis',(0.,1.,0.));
#6888=DIRECTION('ref_axis',(1.,0.,0.));
#6889=DIRECTION('center_axis',(0.,1.,0.));
#6890=DIRECTION('ref_axis',(1.,0.,0.));
#6891=DIRECTION('',(-0.447213595499958,0.894427190999916,-5.47678698264203E-17));
#6892=DIRECTION('center_axis',(0.,-1.,0.));
#6893=DIRECTION('ref_axis',(1.,0.,0.));
#6894=DIRECTION('center_axis',(0.,1.,0.));
#6895=DIRECTION('ref_axis',(1.,0.,0.));
#6896=DIRECTION('',(0.,1.,0.));
#6897=DIRECTION('center_axis',(0.,1.,0.));
#6898=DIRECTION('ref_axis',(1.,0.,0.));
#6899=DIRECTION('center_axis',(0.,-1.,0.));
#6900=DIRECTION('ref_axis',(1.,0.,0.));
#6901=DIRECTION('',(-0.707106781186547,0.707106781186548,-8.65956056235493E-17));
#6902=DIRECTION('center_axis',(0.,-1.,0.));
#6903=DIRECTION('ref_axis',(0.,0.,-1.));
#6904=DIRECTION('center_axis',(0.866025403784439,0.,-0.5));
#6905=DIRECTION('ref_axis',(0.5,0.,0.866025403784439));
#6906=DIRECTION('',(-0.5,0.,-0.866025403784439));
#6907=DIRECTION('',(0.,-1.,0.));
#6908=DIRECTION('',(0.5,0.,0.866025403784439));
#6909=DIRECTION('',(0.,-1.,0.));
#6910=DIRECTION('center_axis',(1.60246890531964E-16,0.,-1.));
#6911=DIRECTION('ref_axis',(1.,0.,1.60246890531964E-16));
#6912=DIRECTION('',(-1.,0.,-1.60246890531964E-16));
#6913=DIRECTION('',(0.,-1.,0.));
#6914=DIRECTION('',(1.,0.,1.60246890531964E-16));
#6915=DIRECTION('center_axis',(-0.866025403784439,0.,-0.5));
#6916=DIRECTION('ref_axis',(0.5,0.,-0.866025403784439));
#6917=DIRECTION('',(-0.5,0.,0.866025403784439));
#6918=DIRECTION('',(0.,-1.,0.));
#6919=DIRECTION('',(0.5,0.,-0.866025403784439));
#6920=DIRECTION('center_axis',(-0.866025403784439,0.,0.5));
#6921=DIRECTION('ref_axis',(-0.5,0.,-0.866025403784439));
#6922=DIRECTION('',(0.5,0.,0.866025403784439));
#6923=DIRECTION('',(0.,-1.,0.));
#6924=DIRECTION('',(-0.5,0.,-0.866025403784439));
#6925=DIRECTION('center_axis',(-1.60246890531964E-16,0.,1.));
#6926=DIRECTION('ref_axis',(-1.,0.,-1.60246890531964E-16));
#6927=DIRECTION('',(1.,0.,1.60246890531964E-16));
#6928=DIRECTION('',(0.,-1.,0.));
#6929=DIRECTION('',(-1.,0.,-1.60246890531964E-16));
#6930=DIRECTION('center_axis',(0.866025403784439,0.,0.5));
#6931=DIRECTION('ref_axis',(-0.5,0.,0.866025403784439));
#6932=DIRECTION('',(0.5,0.,-0.866025403784439));
#6933=DIRECTION('',(-0.5,0.,0.866025403784439));
#6934=DIRECTION('center_axis',(0.,1.,0.));
#6935=DIRECTION('ref_axis',(1.,0.,0.));
#6936=DIRECTION('center_axis',(0.,-1.,0.));
#6937=DIRECTION('ref_axis',(0.,0.,-1.));
#10112=CARTESIAN_POINT('',(0.,0.,0.));
#10113=CARTESIAN_POINT('Origin',(0.3,0.4,0.));
#10114=CARTESIAN_POINT('',(-0.3,0.4,-3.67394039744206E-17));
#10115=CARTESIAN_POINT('Origin',(0.,0.4,0.));
#10116=CARTESIAN_POINT('Origin',(0.,0.375,0.));
#10117=CARTESIAN_POINT('',(-0.35,0.35,-4.28626379701573E-17));
#10118=CARTESIAN_POINT('Origin',(0.,0.35,0.));
#10119=CARTESIAN_POINT('',(-0.325,0.375,-3.9801020972289E-17));
#10120=CARTESIAN_POINT('Origin',(0.,0.19,0.));
#10121=CARTESIAN_POINT('',(-0.35,0.03,-4.28626379701574E-17));
#10122=CARTESIAN_POINT('Origin',(0.,0.03,0.));
#10123=CARTESIAN_POINT('',(-0.35,0.19,-4.28626379701574E-17));
#10124=CARTESIAN_POINT('Origin',(0.,0.0149999999999999,0.));
#10125=CARTESIAN_POINT('',(-0.32,-3.29597460435593E-17,-3.91886975727153E-17));
#10126=CARTESIAN_POINT('Origin',(0.,0.,0.));
#10127=CARTESIAN_POINT('',(-0.335,0.0149999999999999,-4.10256677714363E-17));
#10128=CARTESIAN_POINT('Origin',(0.22,0.,0.));
#10129=CARTESIAN_POINT('',(-0.22,-6.93889390390723E-18,-2.69422295812418E-17));
#10130=CARTESIAN_POINT('Origin',(0.,0.,0.));
#10131=CARTESIAN_POINT('Origin',(0.,-0.02,0.));
#10132=CARTESIAN_POINT('',(-0.1954,-0.0492,2.39295984553393E-17));
#10133=CARTESIAN_POINT('Origin',(0.,-0.0492,0.));
#10134=CARTESIAN_POINT('',(-0.21,-0.02,-2.57175827820944E-17));
#10135=CARTESIAN_POINT('Origin',(0.,-0.8,0.));
#10136=CARTESIAN_POINT('',(-0.1954,-1.5646,2.39295984553393E-17));
#10137=CARTESIAN_POINT('Origin',(0.,-1.5646,0.));
#10138=CARTESIAN_POINT('',(-0.1954,-0.8,-2.39295984553393E-17));
#10139=CARTESIAN_POINT('Origin',(0.,-1.58,0.));
#10140=CARTESIAN_POINT('',(-0.16,-1.6,-1.95943487863577E-17));
#10141=CARTESIAN_POINT('Origin',(0.,-1.6,0.));
#10142=CARTESIAN_POINT('',(-0.18,-1.58,-2.20436423846524E-17));
#10143=CARTESIAN_POINT('Origin',(0.,-1.6,0.));
#10144=CARTESIAN_POINT('Origin',(0.0866025403784439,-0.4,-0.15));
#10145=CARTESIAN_POINT('',(0.173205080756888,-0.4,0.));
#10146=CARTESIAN_POINT('',(0.0866025403784439,-0.4,-0.15));
#10147=CARTESIAN_POINT('',(0.173205080756888,-0.4,0.));
#10148=CARTESIAN_POINT('',(0.0866025403784439,-0.64,-0.15));
#10149=CARTESIAN_POINT('',(0.0866025403784439,-0.4,-0.15));
#10150=CARTESIAN_POINT('',(0.173205080756888,-0.64,0.));
#10151=CARTESIAN_POINT('',(0.173205080756888,-0.64,0.));
#10152=CARTESIAN_POINT('',(0.173205080756888,-0.4,0.));
#10153=CARTESIAN_POINT('Origin',(-0.0866025403784438,-0.4,-0.15));
#10154=CARTESIAN_POINT('',(-0.0866025403784438,-0.4,-0.15));
#10155=CARTESIAN_POINT('',(0.0866025403784439,-0.4,-0.15));
#10156=CARTESIAN_POINT('',(-0.0866025403784438,-0.64,-0.15));
#10157=CARTESIAN_POINT('',(-0.0866025403784438,-0.4,-0.15));
#10158=CARTESIAN_POINT('',(0.0866025403784439,-0.64,-0.15));
#10159=CARTESIAN_POINT('Origin',(-0.173205080756888,-0.4,-2.77555756156289E-17));
#10160=CARTESIAN_POINT('',(-0.173205080756888,-0.4,-2.12115047744981E-17));
#10161=CARTESIAN_POINT('',(-0.0866025403784438,-0.4,-0.15));
#10162=CARTESIAN_POINT('',(-0.173205080756888,-0.64,-2.77555756156289E-17));
#10163=CARTESIAN_POINT('',(-0.173205080756888,-0.4,-2.12115047744981E-17));
#10164=CARTESIAN_POINT('',(-0.0866025403784438,-0.64,-0.15));
#10165=CARTESIAN_POINT('Origin',(-0.0866025403784439,-0.4,0.15));
#10166=CARTESIAN_POINT('',(-0.0866025403784439,-0.4,0.15));
#10167=CARTESIAN_POINT('',(-0.173205080756888,-0.4,-2.12115047744981E-17));
#10168=CARTESIAN_POINT('',(-0.0866025403784439,-0.64,0.15));
#10169=CARTESIAN_POINT('',(-0.0866025403784439,-0.4,0.15));
#10170=CARTESIAN_POINT('',(-0.173205080756888,-0.64,-2.12115047744981E-17));
#10171=CARTESIAN_POINT('Origin',(0.0866025403784439,-0.4,0.15));
#10172=CARTESIAN_POINT('',(0.0866025403784439,-0.4,0.15));
#10173=CARTESIAN_POINT('',(-0.0866025403784439,-0.4,0.15));
#10174=CARTESIAN_POINT('',(0.0866025403784439,-0.64,0.15));
#10175=CARTESIAN_POINT('',(0.0866025403784439,-0.4,0.15));
#10176=CARTESIAN_POINT('',(-0.0866025403784439,-0.64,0.15));
#10177=CARTESIAN_POINT('Origin',(0.173205080756888,-0.4,0.));
#10178=CARTESIAN_POINT('',(0.0866025403784439,-0.4,0.15));
#10179=CARTESIAN_POINT('',(0.0866025403784439,-0.64,0.15));
#10180=CARTESIAN_POINT('Origin',(0.,-0.4,-2.77555756156289E-17));
#10181=CARTESIAN_POINT('Origin',(0.,-0.64,-2.77555756156289E-17));
#10240=UNCERTAINTY_MEASURE_WITH_UNIT(LENGTH_MEASURE(0.001),#10267,
'DISTANCE_ACCURACY_VALUE',
'Maximum model space distance between geometric entities at asserted c
onnectivities');
#10241=UNCERTAINTY_MEASURE_WITH_UNIT(LENGTH_MEASURE(0.001),#10267,
'DISTANCE_ACCURACY_VALUE',
'Maximum model space distance between geometric entities at asserted c
onnectivities');
#10265=(
GEOMETRIC_REPRESENTATION_CONTEXT(3)
GLOBAL_UNCERTAINTY_ASSIGNED_CONTEXT((#10240))
GLOBAL_UNIT_ASSIGNED_CONTEXT((#10267,#10269,#10270))
REPRESENTATION_CONTEXT('','3D')
);
#10266=(
GEOMETRIC_REPRESENTATION_CONTEXT(3)
GLOBAL_UNCERTAINTY_ASSIGNED_CONTEXT((#10241))
GLOBAL_UNIT_ASSIGNED_CONTEXT((#10267,#10269,#10270))
REPRESENTATION_CONTEXT('','3D')
);
#10267=(
LENGTH_UNIT()
NAMED_UNIT(*)
SI_UNIT(.CENTI.,.METRE.)
);
#10269=(
NAMED_UNIT(*)
PLANE_ANGLE_UNIT()
SI_UNIT($,.RADIAN.)
);
#10270=(
NAMED_UNIT(*)
SI_UNIT($,.STERADIAN.)
SOLID_ANGLE_UNIT()
);
#10294=SHAPE_DEFINITION_REPRESENTATION(#10318,#10377);
#10318=PRODUCT_DEFINITION_SHAPE('',$,#10402);
#10377=SHAPE_REPRESENTATION('',(#5495),#10265);
#10378=PRODUCT_DEFINITION_CONTEXT('part definition',#10452,'design');
#10402=PRODUCT_DEFINITION('Cap Screw - M4x16',
'Cap Screw - M4x16',#10426,#10378);
#10426=PRODUCT_DEFINITION_FORMATION('',$,#10477);
#10452=APPLICATION_CONTEXT(
'Core Data for Automotive Mechanical Design Process');
#10453=PRODUCT_CONTEXT('part definition',#10452,'mechanical');
#10477=PRODUCT('Cap Screw - M4x16','Cap Screw - M4x16',
'Cap Screw - M4x16',(#10453));
#10548=COLOUR_RGB('Black',0.12,0.14,0.17);
#10549=FILL_AREA_STYLE_COLOUR('',#10548);
#10550=FILL_AREA_STYLE('',(#10549));
#10551=SURFACE_STYLE_FILL_AREA(#10550);
#10552=SURFACE_SIDE_STYLE('',(#10551));
#10553=SURFACE_STYLE_USAGE(.BOTH.,#10552);
#10554=PRESENTATION_STYLE_ASSIGNMENT((#10553));
ENDSEC;
END-ISO-10303-21;
